ISO-10303-21;
HEADER;
/* Generated by software containing ST-Developer
 * from STEP Tools, Inc. (www.steptools.com) 
 */

FILE_DESCRIPTION(
/* description */ ('Single-Axis Profile-Rail Linear Slide'),
/* implementation_level */ '2;1');

FILE_NAME(
/* name */ 'Cap Screw - M5x20.step',
/* time_stamp */ '2026-10-27T10:47:43-07:00',
/* author */ (''),
/* organization */ (''),
/* preprocessor_version */ 'ST-DEVELOPER v20.2',
/* originating_system */ 'Autodesk Translation Framework v15.17.0.0',
/* authorisation */ '');

FILE_SCHEMA (('AUTOMOTIVE_DESIGN { 1 0 10303 214 3 1 1 }'));
ENDSEC;

DATA;
#10=MECHANICAL_DESIGN_GEOMETRIC_PRESENTATION_REPRESENTATION('',(#351),#14478);
#250=CONICAL_SURFACE('',#9471,0.4,0.785398163397448);
#251=CONICAL_SURFACE('',#9475,0.41,0.785398163397448);
#252=CONICAL_SURFACE('',#9479,0.26,0.463647609000806);
#253=CONICAL_SURFACE('',#9483,0.225,0.785398163397448);
#265=ORIENTED_CLOSED_SHELL('',*,#8614,.F.);
#270=BREP_WITH_VOIDS('Body1',#8613,(#265));
#297=SHAPE_REPRESENTATION_RELATIONSHIP('SRR','None',#14629,#324);
#324=ADVANCED_BREP_SHAPE_REPRESENTATION('',(#270),#14473);
#351=STYLED_ITEM('',(#14838),#270);
#461=FACE_BOUND('',#1778,.T.);
#803=PLANE('',#9469);
#804=PLANE('',#9477);
#805=PLANE('',#9485);
#806=PLANE('',#9486);
#807=PLANE('',#9487);
#808=PLANE('',#9488);
#809=PLANE('',#9489);
#810=PLANE('',#9490);
#811=PLANE('',#9491);
#812=PLANE('',#9492);
#813=PLANE('',#9493);
#1235=FACE_OUTER_BOUND('',#1773,.T.);
#1236=FACE_OUTER_BOUND('',#1774,.T.);
#1237=FACE_OUTER_BOUND('',#1775,.T.);
#1238=FACE_OUTER_BOUND('',#1776,.T.);
#1239=FACE_OUTER_BOUND('',#1777,.T.);
#1240=FACE_OUTER_BOUND('',#1779,.T.);
#1241=FACE_OUTER_BOUND('',#1780,.T.);
#1242=FACE_OUTER_BOUND('',#1781,.T.);
#1243=FACE_OUTER_BOUND('',#1782,.T.);
#1244=FACE_OUTER_BOUND('',#1783,.T.);
#1245=FACE_OUTER_BOUND('',#1784,.T.);
#1246=FACE_OUTER_BOUND('',#1785,.T.);
#1247=FACE_OUTER_BOUND('',#1786,.T.);
#1248=FACE_OUTER_BOUND('',#1787,.T.);
#1249=FACE_OUTER_BOUND('',#1788,.T.);
#1250=FACE_OUTER_BOUND('',#1789,.T.);
#1251=FACE_OUTER_BOUND('',#1790,.T.);
#1773=EDGE_LOOP('',(#7851));
#1774=EDGE_LOOP('',(#7852,#7853,#7854,#7855));
#1775=EDGE_LOOP('',(#7856,#7857,#7858,#7859));
#1776=EDGE_LOOP('',(#7860,#7861,#7862,#7863));
#1777=EDGE_LOOP('',(#7864));
#1778=EDGE_LOOP('',(#7865));
#1779=EDGE_LOOP('',(#7866,#7867,#7868,#7869));
#1780=EDGE_LOOP('',(#7870,#7871,#7872,#7873));
#1781=EDGE_LOOP('',(#7874,#7875,#7876,#7877));
#1782=EDGE_LOOP('',(#7878));
#1783=EDGE_LOOP('',(#7879,#7880,#7881,#7882));
#1784=EDGE_LOOP('',(#7883,#7884,#7885,#7886));
#1785=EDGE_LOOP('',(#7887,#7888,#7889,#7890));
#1786=EDGE_LOOP('',(#7891,#7892,#7893,#7894));
#1787=EDGE_LOOP('',(#7895,#7896,#7897,#7898));
#1788=EDGE_LOOP('',(#7899,#7900,#7901,#7902));
#1789=EDGE_LOOP('',(#7903,#7904,#7905,#7906,#7907,#7908));
#1790=EDGE_LOOP('',(#7909,#7910,#7911,#7912,#7913,#7914));
#2734=LINE('',#14123,#3705);
#2735=LINE('',#14127,#3706);
#2736=LINE('',#14131,#3707);
#2737=LINE('',#14138,#3708);
#2738=LINE('',#14142,#3709);
#2739=LINE('',#14146,#3710);
#2740=LINE('',#14151,#3711);
#2741=LINE('',#14153,#3712);
#2742=LINE('',#14155,#3713);
#2743=LINE('',#14156,#3714);
#2744=LINE('',#14159,#3715);
#2745=LINE('',#14161,#3716);
#2746=LINE('',#14162,#3717);
#2747=LINE('',#14165,#3718);
#2748=LINE('',#14167,#3719);
#2749=LINE('',#14168,#3720);
#2750=LINE('',#14171,#3721);
#2751=LINE('',#14173,#3722);
#2752=LINE('',#14174,#3723);
#2753=LINE('',#14177,#3724);
#2754=LINE('',#14179,#3725);
#2755=LINE('',#14180,#3726);
#2756=LINE('',#14182,#3727);
#2757=LINE('',#14183,#3728);
#3705=VECTOR('',#11623,0.4);
#3706=VECTOR('',#11628,0.425);
#3707=VECTOR('',#11633,0.41);
#3708=VECTOR('',#11642,0.26);
#3709=VECTOR('',#11647,0.25);
#3710=VECTOR('',#11652,0.225);
#3711=VECTOR('',#11657,1.);
#3712=VECTOR('',#11658,1.);
#3713=VECTOR('',#11659,1.);
#3714=VECTOR('',#11660,1.);
#3715=VECTOR('',#11663,1.);
#3716=VECTOR('',#11664,1.);
#3717=VECTOR('',#11665,1.);
#3718=VECTOR('',#11668,1.);
#3719=VECTOR('',#11669,1.);
#3720=VECTOR('',#11670,1.);
#3721=VECTOR('',#11673,1.);
#3722=VECTOR('',#11674,1.);
#3723=VECTOR('',#11675,1.);
#3724=VECTOR('',#11678,1.);
#3725=VECTOR('',#11679,1.);
#3726=VECTOR('',#11680,1.);
#3727=VECTOR('',#11683,1.);
#3728=VECTOR('',#11684,1.);
#3905=CIRCLE('',#9470,0.375);
#3906=CIRCLE('',#9472,0.425);
#3907=CIRCLE('',#9474,0.425);
#3908=CIRCLE('',#9476,0.395);
#3909=CIRCLE('',#9478,0.27);
#3910=CIRCLE('',#9480,0.24505);
#3911=CIRCLE('',#9482,0.24505);
#3912=CIRCLE('',#9484,0.2);
#4615=VERTEX_POINT('',#14118);
#4616=VERTEX_POINT('',#14121);
#4617=VERTEX_POINT('',#14125);
#4618=VERTEX_POINT('',#14129);
#4619=VERTEX_POINT('',#14133);
#4620=VERTEX_POINT('',#14136);
#4621=VERTEX_POINT('',#14140);
#4622=VERTEX_POINT('',#14144);
#4623=VERTEX_POINT('',#14149);
#4624=VERTEX_POINT('',#14150);
#4625=VERTEX_POINT('',#14152);
#4626=VERTEX_POINT('',#14154);
#4627=VERTEX_POINT('',#14158);
#4628=VERTEX_POINT('',#14160);
#4629=VERTEX_POINT('',#14164);
#4630=VERTEX_POINT('',#14166);
#4631=VERTEX_POINT('',#14170);
#4632=VERTEX_POINT('',#14172);
#4633=VERTEX_POINT('',#14176);
#4634=VERTEX_POINT('',#14178);
#5703=EDGE_CURVE('',#4615,#4615,#3905,.T.);
#5704=EDGE_CURVE('',#4616,#4616,#3906,.T.);
#5705=EDGE_CURVE('',#4616,#4615,#2734,.T.);
#5706=EDGE_CURVE('',#4617,#4617,#3907,.T.);
#5707=EDGE_CURVE('',#4617,#4616,#2735,.T.);
#5708=EDGE_CURVE('',#4618,#4618,#3908,.T.);
#5709=EDGE_CURVE('',#4618,#4617,#2736,.T.);
#5710=EDGE_CURVE('',#4619,#4619,#3909,.T.);
#5711=EDGE_CURVE('',#4620,#4620,#3910,.F.);
#5712=EDGE_CURVE('',#4620,#4619,#2737,.T.);
#5713=EDGE_CURVE('',#4621,#4621,#3911,.F.);
#5714=EDGE_CURVE('',#4621,#4620,#2738,.T.);
#5715=EDGE_CURVE('',#4622,#4622,#3912,.T.);
#5716=EDGE_CURVE('',#4622,#4621,#2739,.T.);
#5717=EDGE_CURVE('',#4623,#4624,#2740,.T.);
#5718=EDGE_CURVE('',#4624,#4625,#2741,.T.);
#5719=EDGE_CURVE('',#4625,#4626,#2742,.T.);
#5720=EDGE_CURVE('',#4623,#4626,#2743,.T.);
#5721=EDGE_CURVE('',#4624,#4627,#2744,.T.);
#5722=EDGE_CURVE('',#4627,#4628,#2745,.T.);
#5723=EDGE_CURVE('',#4628,#4625,#2746,.T.);
#5724=EDGE_CURVE('',#4627,#4629,#2747,.T.);
#5725=EDGE_CURVE('',#4629,#4630,#2748,.T.);
#5726=EDGE_CURVE('',#4630,#4628,#2749,.T.);
#5727=EDGE_CURVE('',#4629,#4631,#2750,.T.);
#5728=EDGE_CURVE('',#4631,#4632,#2751,.T.);
#5729=EDGE_CURVE('',#4632,#4630,#2752,.T.);
#5730=EDGE_CURVE('',#4631,#4633,#2753,.T.);
#5731=EDGE_CURVE('',#4633,#4634,#2754,.T.);
#5732=EDGE_CURVE('',#4634,#4632,#2755,.T.);
#5733=EDGE_CURVE('',#4633,#4623,#2756,.T.);
#5734=EDGE_CURVE('',#4626,#4634,#2757,.T.);
#7851=ORIENTED_EDGE('',*,*,#5703,.F.);
#7852=ORIENTED_EDGE('',*,*,#5704,.F.);
#7853=ORIENTED_EDGE('',*,*,#5705,.T.);
#7854=ORIENTED_EDGE('',*,*,#5703,.T.);
#7855=ORIENTED_EDGE('',*,*,#5705,.F.);
#7856=ORIENTED_EDGE('',*,*,#5706,.F.);
#7857=ORIENTED_EDGE('',*,*,#5707,.T.);
#7858=ORIENTED_EDGE('',*,*,#5704,.T.);
#7859=ORIENTED_EDGE('',*,*,#5707,.F.);
#7860=ORIENTED_EDGE('',*,*,#5708,.F.);
#7861=ORIENTED_EDGE('',*,*,#5709,.T.);
#7862=ORIENTED_EDGE('',*,*,#5706,.T.);
#7863=ORIENTED_EDGE('',*,*,#5709,.F.);
#7864=ORIENTED_EDGE('',*,*,#5708,.T.);
#7865=ORIENTED_EDGE('',*,*,#5710,.F.);
#7866=ORIENTED_EDGE('',*,*,#5711,.F.);
#7867=ORIENTED_EDGE('',*,*,#5712,.T.);
#7868=ORIENTED_EDGE('',*,*,#5710,.T.);
#7869=ORIENTED_EDGE('',*,*,#5712,.F.);
#7870=ORIENTED_EDGE('',*,*,#5713,.F.);
#7871=ORIENTED_EDGE('',*,*,#5714,.T.);
#7872=ORIENTED_EDGE('',*,*,#5711,.T.);
#7873=ORIENTED_EDGE('',*,*,#5714,.F.);
#7874=ORIENTED_EDGE('',*,*,#5715,.F.);
#7875=ORIENTED_EDGE('',*,*,#5716,.T.);
#7876=ORIENTED_EDGE('',*,*,#5713,.T.);
#7877=ORIENTED_EDGE('',*,*,#5716,.F.);
#7878=ORIENTED_EDGE('',*,*,#5715,.T.);
#7879=ORIENTED_EDGE('',*,*,#5717,.T.);
#7880=ORIENTED_EDGE('',*,*,#5718,.T.);
#7881=ORIENTED_EDGE('',*,*,#5719,.T.);
#7882=ORIENTED_EDGE('',*,*,#5720,.F.);
#7883=ORIENTED_EDGE('',*,*,#5721,.T.);
#7884=ORIENTED_EDGE('',*,*,#5722,.T.);
#7885=ORIENTED_EDGE('',*,*,#5723,.T.);
#7886=ORIENTED_EDGE('',*,*,#5718,.F.);
#7887=ORIENTED_EDGE('',*,*,#5724,.T.);
#7888=ORIENTED_EDGE('',*,*,#5725,.T.);
#7889=ORIENTED_EDGE('',*,*,#5726,.T.);
#7890=ORIENTED_EDGE('',*,*,#5722,.F.);
#7891=ORIENTED_EDGE('',*,*,#5727,.T.);
#7892=ORIENTED_EDGE('',*,*,#5728,.T.);
#7893=ORIENTED_EDGE('',*,*,#5729,.T.);
#7894=ORIENTED_EDGE('',*,*,#5725,.F.);
#7895=ORIENTED_EDGE('',*,*,#5730,.T.);
#7896=ORIENTED_EDGE('',*,*,#5731,.T.);
#7897=ORIENTED_EDGE('',*,*,#5732,.T.);
#7898=ORIENTED_EDGE('',*,*,#5728,.F.);
#7899=ORIENTED_EDGE('',*,*,#5733,.T.);
#7900=ORIENTED_EDGE('',*,*,#5720,.T.);
#7901=ORIENTED_EDGE('',*,*,#5734,.T.);
#7902=ORIENTED_EDGE('',*,*,#5731,.F.);
#7903=ORIENTED_EDGE('',*,*,#5733,.F.);
#7904=ORIENTED_EDGE('',*,*,#5730,.F.);
#7905=ORIENTED_EDGE('',*,*,#5727,.F.);
#7906=ORIENTED_EDGE('',*,*,#5724,.F.);
#7907=ORIENTED_EDGE('',*,*,#5721,.F.);
#7908=ORIENTED_EDGE('',*,*,#5717,.F.);
#7909=ORIENTED_EDGE('',*,*,#5734,.F.);
#7910=ORIENTED_EDGE('',*,*,#5719,.F.);
#7911=ORIENTED_EDGE('',*,*,#5723,.F.);
#7912=ORIENTED_EDGE('',*,*,#5726,.F.);
#7913=ORIENTED_EDGE('',*,*,#5729,.F.);
#7914=ORIENTED_EDGE('',*,*,#5732,.F.);
#8124=CYLINDRICAL_SURFACE('',#9473,0.425);
#8125=CYLINDRICAL_SURFACE('',#9481,0.24505);
#8529=ADVANCED_FACE('',(#1235),#803,.T.);
#8530=ADVANCED_FACE('',(#1236),#250,.T.);
#8531=ADVANCED_FACE('',(#1237),#8124,.T.);
#8532=ADVANCED_FACE('',(#1238),#251,.T.);
#8533=ADVANCED_FACE('',(#1239,#461),#804,.T.);
#8534=ADVANCED_FACE('',(#1240),#252,.T.);
#8535=ADVANCED_FACE('',(#1241),#8125,.T.);
#8536=ADVANCED_FACE('',(#1242),#253,.T.);
#8537=ADVANCED_FACE('',(#1243),#805,.T.);
#8538=ADVANCED_FACE('',(#1244),#806,.F.);
#8539=ADVANCED_FACE('',(#1245),#807,.F.);
#8540=ADVANCED_FACE('',(#1246),#808,.F.);
#8541=ADVANCED_FACE('',(#1247),#809,.F.);
#8542=ADVANCED_FACE('',(#1248),#810,.F.);
#8543=ADVANCED_FACE('',(#1249),#811,.F.);
#8544=ADVANCED_FACE('',(#1250),#812,.F.);
#8545=ADVANCED_FACE('',(#1251),#813,.F.);
#8613=CLOSED_SHELL('',(#8529,#8530,#8531,#8532,#8533,#8534,#8535,#8536,
#8537));
#8614=CLOSED_SHELL('',(#8538,#8539,#8540,#8541,#8542,#8543,#8544,#8545));
#9468=AXIS2_PLACEMENT_3D('',#14116,#11613,#11614);
#9469=AXIS2_PLACEMENT_3D('',#14117,#11615,#11616);
#9470=AXIS2_PLACEMENT_3D('',#14119,#11617,#11618);
#9471=AXIS2_PLACEMENT_3D('',#14120,#11619,#11620);
#9472=AXIS2_PLACEMENT_3D('',#14122,#11621,#11622);
#9473=AXIS2_PLACEMENT_3D('',#14124,#11624,#11625);
#9474=AXIS2_PLACEMENT_3D('',#14126,#11626,#11627);
#9475=AXIS2_PLACEMENT_3D('',#14128,#11629,#11630);
#9476=AXIS2_PLACEMENT_3D('',#14130,#11631,#11632);
#9477=AXIS2_PLACEMENT_3D('',#14132,#11634,#11635);
#9478=AXIS2_PLACEMENT_3D('',#14134,#11636,#11637);
#9479=AXIS2_PLACEMENT_3D('',#14135,#11638,#11639);
#9480=AXIS2_PLACEMENT_3D('',#14137,#11640,#11641);
#9481=AXIS2_PLACEMENT_3D('',#14139,#11643,#11644);
#9482=AXIS2_PLACEMENT_3D('',#14141,#11645,#11646);
#9483=AXIS2_PLACEMENT_3D('',#14143,#11648,#11649);
#9484=AXIS2_PLACEMENT_3D('',#14145,#11650,#11651);
#9485=AXIS2_PLACEMENT_3D('',#14147,#11653,#11654);
#9486=AXIS2_PLACEMENT_3D('',#14148,#11655,#11656);
#9487=AXIS2_PLACEMENT_3D('',#14157,#11661,#11662);
#9488=AXIS2_PLACEMENT_3D('',#14163,#11666,#11667);
#9489=AXIS2_PLACEMENT_3D('',#14169,#11671,#11672);
#9490=AXIS2_PLACEMENT_3D('',#14175,#11676,#11677);
#9491=AXIS2_PLACEMENT_3D('',#14181,#11681,#11682);
#9492=AXIS2_PLACEMENT_3D('',#14184,#11685,#11686);
#9493=AXIS2_PLACEMENT_3D('',#14185,#11687,#11688);
#11613=DIRECTION('axis',(0.,0.,1.));
#11614=DIRECTION('refdir',(1.,0.,0.));
#11615=DIRECTION('center_axis',(0.,1.,0.));
#11616=DIRECTION('ref_axis',(0.,0.,1.));
#11617=DIRECTION('center_axis',(0.,-1.,0.));
#11618=DIRECTION('ref_axis',(1.,0.,0.));
#11619=DIRECTION('center_axis',(0.,-1.,0.));
#11620=DIRECTION('ref_axis',(1.,0.,0.));
#11621=DIRECTION('center_axis',(0.,-1.,0.));
#11622=DIRECTION('ref_axis',(1.,0.,0.));
#11623=DIRECTION('',(0.707106781186548,0.707106781186547,8.65956056235493E-17));
#11624=DIRECTION('center_axis',(0.,-1.,0.));
#11625=DIRECTION('ref_axis',(1.,0.,0.));
#11626=DIRECTION('center_axis',(0.,-1.,0.));
#11627=DIRECTION('ref_axis',(1.,0.,0.));
#11628=DIRECTION('',(0.,1.,0.));
#11629=DIRECTION('center_axis',(0.,1.,0.));
#11630=DIRECTION('ref_axis',(1.,0.,0.));
#11631=DIRECTION('center_axis',(0.,-1.,0.));
#11632=DIRECTION('ref_axis',(1.,0.,0.));
#11633=DIRECTION('',(-0.707106781186547,0.707106781186548,-8.65956056235493E-17));
#11634=DIRECTION('center_axis',(0.,-1.,0.));
#11635=DIRECTION('ref_axis',(0.,0.,-1.));
#11636=DIRECTION('center_axis',(0.,-1.,0.));
#11637=DIRECTION('ref_axis',(1.,0.,0.));
#11638=DIRECTION('center_axis',(0.,1.,0.));
#11639=DIRECTION('ref_axis',(1.,0.,0.));
#11640=DIRECTION('center_axis',(0.,1.,0.));
#11641=DIRECTION('ref_axis',(1.,0.,0.));
#11642=DIRECTION('',(-0.447213595499958,0.894427190999916,-5.47678698264203E-17));
#11643=DIRECTION('center_axis',(0.,-1.,0.));
#11644=DIRECTION('ref_axis',(1.,0.,0.));
#11645=DIRECTION('center_axis',(0.,1.,0.));
#11646=DIRECTION('ref_axis',(1.,0.,0.));
#11647=DIRECTION('',(0.,1.,0.));
#11648=DIRECTION('center_axis',(0.,1.,0.));
#11649=DIRECTION('ref_axis',(1.,0.,0.));
#11650=DIRECTION('center_axis',(0.,-1.,0.));
#11651=DIRECTION('ref_axis',(1.,0.,0.));
#11652=DIRECTION('',(-0.707106781186547,0.707106781186548,-8.65956056235493E-17));
#11653=DIRECTION('center_axis',(0.,-1.,0.));
#11654=DIRECTION('ref_axis',(0.,0.,-1.));
#11655=DIRECTION('center_axis',(0.866025403784439,0.,-0.5));
#11656=DIRECTION('ref_axis',(0.5,0.,0.866025403784439));
#11657=DIRECTION('',(-0.5,0.,-0.866025403784439));
#11658=DIRECTION('',(0.,-1.,0.));
#11659=DIRECTION('',(0.5,0.,0.866025403784439));
#11660=DIRECTION('',(0.,-1.,0.));
#11661=DIRECTION('center_axis',(1.20185167898973E-16,0.,-1.));
#11662=DIRECTION('ref_axis',(1.,0.,1.20185167898973E-16));
#11663=DIRECTION('',(-1.,0.,-1.20185167898973E-16));
#11664=DIRECTION('',(0.,-1.,0.));
#11665=DIRECTION('',(1.,0.,1.20185167898973E-16));
#11666=DIRECTION('center_axis',(-0.866025403784439,0.,-0.5));
#11667=DIRECTION('ref_axis',(0.5,0.,-0.866025403784439));
#11668=DIRECTION('',(-0.5,0.,0.866025403784439));
#11669=DIRECTION('',(0.,-1.,0.));
#11670=DIRECTION('',(0.5,0.,-0.866025403784439));
#11671=DIRECTION('center_axis',(-0.866025403784439,0.,0.5));
#11672=DIRECTION('ref_axis',(-0.5,0.,-0.866025403784439));
#11673=DIRECTION('',(0.5,0.,0.866025403784439));
#11674=DIRECTION('',(0.,-1.,0.));
#11675=DIRECTION('',(-0.5,0.,-0.866025403784439));
#11676=DIRECTION('center_axis',(-2.40370335797945E-16,0.,1.));
#11677=DIRECTION('ref_axis',(-1.,0.,-2.40370335797945E-16));
#11678=DIRECTION('',(1.,0.,2.40370335797945E-16));
#11679=DIRECTION('',(0.,-1.,0.));
#11680=DIRECTION('',(-1.,0.,-2.40370335797945E-16));
#11681=DIRECTION('center_axis',(0.866025403784439,0.,0.5));
#11682=DIRECTION('ref_axis',(-0.5,0.,0.866025403784439));
#11683=DIRECTION('',(0.5,0.,-0.866025403784439));
#11684=DIRECTION('',(-0.5,0.,0.866025403784439));
#11685=DIRECTION('center_axis',(0.,1.,0.));
#11686=DIRECTION('ref_axis',(1.,0.,0.));
#11687=DIRECTION('center_axis',(0.,-1.,0.));
#11688=DIRECTION('ref_axis',(0.,0.,-1.));
#14116=CARTESIAN_POINT('',(0.,0.,0.));
#14117=CARTESIAN_POINT('Origin',(0.375,0.5,0.));
#14118=CARTESIAN_POINT('',(-0.375,0.5,-4.59242549680257E-17));
#14119=CARTESIAN_POINT('Origin',(0.,0.5,0.));
#14120=CARTESIAN_POINT('Origin',(0.,0.475,0.));
#14121=CARTESIAN_POINT('',(-0.425,0.45,-5.20474889637625E-17));
#14122=CARTESIAN_POINT('Origin',(0.,0.45,0.));
#14123=CARTESIAN_POINT('',(-0.4,0.475,-4.89858719658941E-17));
#14124=CARTESIAN_POINT('Origin',(0.,0.24,0.));
#14125=CARTESIAN_POINT('',(-0.425,0.0299999999999998,-5.20474889637625E-17));
#14126=CARTESIAN_POINT('Origin',(0.,0.0299999999999998,0.));
#14127=CARTESIAN_POINT('',(-0.425,0.24,-5.20474889637625E-17));
#14128=CARTESIAN_POINT('Origin',(0.,0.0150000000000001,0.));
#14129=CARTESIAN_POINT('',(-0.395,4.85722573273506E-17,-4.83735485663204E-17));
#14130=CARTESIAN_POINT('Origin',(0.,0.,0.));
#14131=CARTESIAN_POINT('',(-0.41,0.0150000000000001,-5.02105187650415E-17));
#14132=CARTESIAN_POINT('Origin',(0.27,0.,0.));
#14133=CARTESIAN_POINT('',(-0.27,0.,-3.30654635769785E-17));
#14134=CARTESIAN_POINT('Origin',(0.,0.,0.));
#14135=CARTESIAN_POINT('Origin',(0.,-0.02,0.));
#14136=CARTESIAN_POINT('',(-0.24505,-0.0498999999999999,3.00099698131059E-17));
#14137=CARTESIAN_POINT('Origin',(0.,-0.0498999999999999,0.));
#14138=CARTESIAN_POINT('',(-0.26,-0.02,-3.18408167778312E-17));
#14139=CARTESIAN_POINT('Origin',(0.,-0.995,0.));
#14140=CARTESIAN_POINT('',(-0.24505,-1.95495,3.00099698131059E-17));
#14141=CARTESIAN_POINT('Origin',(0.,-1.95495,0.));
#14142=CARTESIAN_POINT('',(-0.24505,-0.995,-3.00099698131059E-17));
#14143=CARTESIAN_POINT('Origin',(0.,-1.975,0.));
#14144=CARTESIAN_POINT('',(-0.2,-2.,-2.44929359829471E-17));
#14145=CARTESIAN_POINT('Origin',(0.,-2.,0.));
#14146=CARTESIAN_POINT('',(-0.225,-1.975,-2.75545529808154E-17));
#14147=CARTESIAN_POINT('Origin',(0.,-2.,0.));
#14148=CARTESIAN_POINT('Origin',(0.115470053837925,-0.5,-0.2));
#14149=CARTESIAN_POINT('',(0.23094010767585,-0.5,0.));
#14150=CARTESIAN_POINT('',(0.115470053837925,-0.5,-0.2));
#14151=CARTESIAN_POINT('',(0.23094010767585,-0.5,0.));
#14152=CARTESIAN_POINT('',(0.115470053837925,-0.8,-0.2));
#14153=CARTESIAN_POINT('',(0.115470053837925,-0.5,-0.2));
#14154=CARTESIAN_POINT('',(0.23094010767585,-0.8,0.));
#14155=CARTESIAN_POINT('',(0.23094010767585,-0.8,0.));
#14156=CARTESIAN_POINT('',(0.23094010767585,-0.5,0.));
#14157=CARTESIAN_POINT('Origin',(-0.115470053837925,-0.5,-0.2));
#14158=CARTESIAN_POINT('',(-0.115470053837925,-0.5,-0.2));
#14159=CARTESIAN_POINT('',(0.115470053837925,-0.5,-0.2));
#14160=CARTESIAN_POINT('',(-0.115470053837925,-0.8,-0.2));
#14161=CARTESIAN_POINT('',(-0.115470053837925,-0.5,-0.2));
#14162=CARTESIAN_POINT('',(0.115470053837925,-0.8,-0.2));
#14163=CARTESIAN_POINT('Origin',(-0.23094010767585,-0.5,-2.77555756156289E-17));
#14164=CARTESIAN_POINT('',(-0.23094010767585,-0.5,-2.82820063659975E-17));
#14165=CARTESIAN_POINT('',(-0.115470053837925,-0.5,-0.2));
#14166=CARTESIAN_POINT('',(-0.23094010767585,-0.8,-2.77555756156289E-17));
#14167=CARTESIAN_POINT('',(-0.23094010767585,-0.5,-2.82820063659975E-17));
#14168=CARTESIAN_POINT('',(-0.115470053837925,-0.8,-0.2));
#14169=CARTESIAN_POINT('Origin',(-0.115470053837925,-0.5,0.2));
#14170=CARTESIAN_POINT('',(-0.115470053837925,-0.5,0.2));
#14171=CARTESIAN_POINT('',(-0.23094010767585,-0.5,-2.82820063659975E-17));
#14172=CARTESIAN_POINT('',(-0.115470053837925,-0.8,0.2));
#14173=CARTESIAN_POINT('',(-0.115470053837925,-0.5,0.2));
#14174=CARTESIAN_POINT('',(-0.23094010767585,-0.8,-2.82820063659975E-17));
#14175=CARTESIAN_POINT('Origin',(0.115470053837925,-0.5,0.2));
#14176=CARTESIAN_POINT('',(0.115470053837925,-0.5,0.2));
#14177=CARTESIAN_POINT('',(-0.115470053837925,-0.5,0.2));
#14178=CARTESIAN_POINT('',(0.115470053837925,-0.8,0.2));
#14179=CARTESIAN_POINT('',(0.115470053837925,-0.5,0.2));
#14180=CARTESIAN_POINT('',(-0.115470053837925,-0.8,0.2));
#14181=CARTESIAN_POINT('Origin',(0.23094010767585,-0.5,0.));
#14182=CARTESIAN_POINT('',(0.115470053837925,-0.5,0.2));
#14183=CARTESIAN_POINT('',(0.115470053837925,-0.8,0.2));
#14184=CARTESIAN_POINT('Origin',(0.,-0.5,0.));
#14185=CARTESIAN_POINT('Origin',(0.,-0.8,0.));
#14441=UNCERTAINTY_MEASURE_WITH_UNIT(LENGTH_MEASURE(0.001),#14479,
'DISTANCE_ACCURACY_VALUE',
'Maximum model space distance between geometric entities at asserted c
onnectivities');
#14446=UNCERTAINTY_MEASURE_WITH_UNIT(LENGTH_MEASURE(0.001),#14479,
'DISTANCE_ACCURACY_VALUE',
'Maximum model space distance between geometric entities at asserted c
onnectivities');
#14473=(
GEOMETRIC_REPRESENTATION_CONTEXT(3)
GLOBAL_UNCERTAINTY_ASSIGNED_CONTEXT((#14441))
GLOBAL_UNIT_ASSIGNED_CONTEXT((#14479,#14481,#14482))
REPRESENTATION_CONTEXT('','3D')
);
#14478=(
GEOMETRIC_REPRESENTATION_CONTEXT(3)
GLOBAL_UNCERTAINTY_ASSIGNED_CONTEXT((#14446))
GLOBAL_UNIT_ASSIGNED_CONTEXT((#14479,#14481,#14482))
REPRESENTATION_CONTEXT('','3D')
);
#14479=(
LENGTH_UNIT()
NAMED_UNIT(*)
SI_UNIT(.CENTI.,.METRE.)
);
#14481=(
NAMED_UNIT(*)
PLANE_ANGLE_UNIT()
SI_UNIT($,.RADIAN.)
);
#14482=(
NAMED_UNIT(*)
SI_UNIT($,.STERADIAN.)
SOLID_ANGLE_UNIT()
);
#14509=SHAPE_DEFINITION_REPRESENTATION(#14543,#14629);
#14543=PRODUCT_DEFINITION_SHAPE('',$,#14661);
#14629=SHAPE_REPRESENTATION('',(#9468),#14473);
#14634=PRODUCT_DEFINITION_CONTEXT('part definition',#14729,'design');
#14661=PRODUCT_DEFINITION('Cap Screw - M5x20','Cap Screw - M5x20',#14692,
#14634);
#14692=PRODUCT_DEFINITION_FORMATION('',$,#14757);
#14729=APPLICATION_CONTEXT(
'Core Data for Automotive Mechanical Design Process');
#14730=PRODUCT_CONTEXT('part definition',#14729,'mechanical');
#14757=PRODUCT('Cap Screw - M5x20','Cap Screw - M5x20',
'Cap Screw - M5x20',(#14730));
#14832=COLOUR_RGB('Black',0.12,0.14,0.17);
#14833=FILL_AREA_STYLE_COLOUR('',#14832);
#14834=FILL_AREA_STYLE('',(#14833));
#14835=SURFACE_STYLE_FILL_AREA(#14834);
#14836=SURFACE_SIDE_STYLE('',(#14835));
#14837=SURFACE_STYLE_USAGE(.BOTH.,#14836);
#14838=PRESENTATION_STYLE_ASSIGNMENT((#14837));
ENDSEC;
END-ISO-10303-21;
